ISO-10303-21;
HEADER;
/* Generated by software containing ST-Developer
 * from STEP Tools, Inc. (www.steptools.com) 
 */

FILE_DESCRIPTION(
/* description */ (''),
/* implementation_level */ '2;1');

FILE_NAME(
/* name */ 'Screw_01.step',
/* time_stamp */ '2026-10-05T21:34:53-07:00',
/* author */ (''),
/* organization */ (''),
/* preprocessor_version */ 'ST-DEVELOPER v20.2',
/* originating_system */ 'Autodesk Translation Framework v15.15.0.0',
/* authorisation */ '');

FILE_SCHEMA (('AUTOMOTIVE_DESIGN { 1 0 10303 214 3 1 1 }'));
ENDSEC;

DATA;
#10=MECHANICAL_DESIGN_GEOMETRIC_PRESENTATION_REPRESENTATION('',(#68),#9822);
#50=SHAPE_REPRESENTATION_RELATIONSHIP('SRR','None',#9860,#59);
#59=ADVANCED_BREP_SHAPE_REPRESENTATION('',(#77),#9816);
#68=STYLED_ITEM('',(#9912),#77);
#77=MANIFOLD_SOLID_BREP('Body1',#3291);
#95=FACE_BOUND('',#608,.T.);
#229=PLANE('',#3645);
#230=PLANE('',#3646);
#231=PLANE('',#3647);
#232=PLANE('',#3648);
#233=PLANE('',#3649);
#234=PLANE('',#3650);
#235=PLANE('',#3651);
#236=PLANE('',#3655);
#237=PLANE('',#3656);
#402=FACE_OUTER_BOUND('',#599,.T.);
#403=FACE_OUTER_BOUND('',#600,.T.);
#404=FACE_OUTER_BOUND('',#601,.T.);
#405=FACE_OUTER_BOUND('',#602,.T.);
#406=FACE_OUTER_BOUND('',#603,.T.);
#407=FACE_OUTER_BOUND('',#604,.T.);
#408=FACE_OUTER_BOUND('',#605,.T.);
#409=FACE_OUTER_BOUND('',#606,.T.);
#410=FACE_OUTER_BOUND('',#607,.T.);
#411=FACE_OUTER_BOUND('',#609,.T.);
#599=EDGE_LOOP('',(#2834,#2835,#2836,#2837));
#600=EDGE_LOOP('',(#2838,#2839,#2840,#2841));
#601=EDGE_LOOP('',(#2842,#2843,#2844,#2845));
#602=EDGE_LOOP('',(#2846,#2847,#2848,#2849));
#603=EDGE_LOOP('',(#2850,#2851,#2852,#2853));
#604=EDGE_LOOP('',(#2854,#2855,#2856,#2857));
#605=EDGE_LOOP('',(#2858,#2859,#2860,#2861,#2862,#2863));
#606=EDGE_LOOP('',(#2864,#2865,#2866,#2867));
#607=EDGE_LOOP('',(#2868));
#608=EDGE_LOOP('',(#2869,#2870,#2871,#2872,#2873,#2874));
#609=EDGE_LOOP('',(#2875));
#838=LINE('',#9514,#1097);
#839=LINE('',#9516,#1098);
#840=LINE('',#9518,#1099);
#841=LINE('',#9519,#1100);
#842=LINE('',#9522,#1101);
#843=LINE('',#9524,#1102);
#844=LINE('',#9525,#1103);
#845=LINE('',#9528,#1104);
#846=LINE('',#9530,#1105);
#847=LINE('',#9531,#1106);
#848=LINE('',#9534,#1107);
#849=LINE('',#9536,#1108);
#850=LINE('',#9537,#1109);
#851=LINE('',#9540,#1110);
#852=LINE('',#9542,#1111);
#853=LINE('',#9543,#1112);
#854=LINE('',#9545,#1113);
#855=LINE('',#9546,#1114);
#856=LINE('',#9552,#1115);
#1097=VECTOR('',#4412,10.);
#1098=VECTOR('',#4413,10.);
#1099=VECTOR('',#4414,10.);
#1100=VECTOR('',#4415,10.);
#1101=VECTOR('',#4418,10.);
#1102=VECTOR('',#4419,10.);
#1103=VECTOR('',#4420,10.);
#1104=VECTOR('',#4423,10.);
#1105=VECTOR('',#4424,10.);
#1106=VECTOR('',#4425,10.);
#1107=VECTOR('',#4428,9.99999999999999);
#1108=VECTOR('',#4429,10.);
#1109=VECTOR('',#4430,9.99999999999999);
#1110=VECTOR('',#4433,10.);
#1111=VECTOR('',#4434,10.);
#1112=VECTOR('',#4435,10.);
#1113=VECTOR('',#4438,10.);
#1114=VECTOR('',#4439,10.);
#1115=VECTOR('',#4446,1.);
#1299=CIRCLE('',#3653,1.);
#1300=CIRCLE('',#3654,1.);
#1561=VERTEX_POINT('',#9512);
#1562=VERTEX_POINT('',#9513);
#1563=VERTEX_POINT('',#9515);
#1564=VERTEX_POINT('',#9517);
#1565=VERTEX_POINT('',#9521);
#1566=VERTEX_POINT('',#9523);
#1567=VERTEX_POINT('',#9527);
#1568=VERTEX_POINT('',#9529);
#1569=VERTEX_POINT('',#9533);
#1570=VERTEX_POINT('',#9535);
#1571=VERTEX_POINT('',#9539);
#1572=VERTEX_POINT('',#9541);
#1573=VERTEX_POINT('',#9549);
#1574=VERTEX_POINT('',#9551);
#1996=EDGE_CURVE('',#1561,#1562,#838,.T.);
#1997=EDGE_CURVE('',#1561,#1563,#839,.T.);
#1998=EDGE_CURVE('',#1563,#1564,#840,.T.);
#1999=EDGE_CURVE('',#1562,#1564,#841,.T.);
#2000=EDGE_CURVE('',#1565,#1561,#842,.T.);
#2001=EDGE_CURVE('',#1565,#1566,#843,.T.);
#2002=EDGE_CURVE('',#1566,#1563,#844,.T.);
#2003=EDGE_CURVE('',#1567,#1565,#845,.T.);
#2004=EDGE_CURVE('',#1567,#1568,#846,.T.);
#2005=EDGE_CURVE('',#1568,#1566,#847,.T.);
#2006=EDGE_CURVE('',#1569,#1567,#848,.T.);
#2007=EDGE_CURVE('',#1569,#1570,#849,.T.);
#2008=EDGE_CURVE('',#1570,#1568,#850,.T.);
#2009=EDGE_CURVE('',#1571,#1569,#851,.T.);
#2010=EDGE_CURVE('',#1571,#1572,#852,.T.);
#2011=EDGE_CURVE('',#1572,#1570,#853,.T.);
#2012=EDGE_CURVE('',#1562,#1571,#854,.T.);
#2013=EDGE_CURVE('',#1564,#1572,#855,.T.);
#2014=EDGE_CURVE('',#1573,#1573,#1299,.T.);
#2015=EDGE_CURVE('',#1573,#1574,#856,.T.);
#2016=EDGE_CURVE('',#1574,#1574,#1300,.T.);
#2834=ORIENTED_EDGE('',*,*,#1996,.F.);
#2835=ORIENTED_EDGE('',*,*,#1997,.T.);
#2836=ORIENTED_EDGE('',*,*,#1998,.T.);
#2837=ORIENTED_EDGE('',*,*,#1999,.F.);
#2838=ORIENTED_EDGE('',*,*,#2000,.F.);
#2839=ORIENTED_EDGE('',*,*,#2001,.T.);
#2840=ORIENTED_EDGE('',*,*,#2002,.T.);
#2841=ORIENTED_EDGE('',*,*,#1997,.F.);
#2842=ORIENTED_EDGE('',*,*,#2003,.F.);
#2843=ORIENTED_EDGE('',*,*,#2004,.T.);
#2844=ORIENTED_EDGE('',*,*,#2005,.T.);
#2845=ORIENTED_EDGE('',*,*,#2001,.F.);
#2846=ORIENTED_EDGE('',*,*,#2006,.F.);
#2847=ORIENTED_EDGE('',*,*,#2007,.T.);
#2848=ORIENTED_EDGE('',*,*,#2008,.T.);
#2849=ORIENTED_EDGE('',*,*,#2004,.F.);
#2850=ORIENTED_EDGE('',*,*,#2009,.F.);
#2851=ORIENTED_EDGE('',*,*,#2010,.T.);
#2852=ORIENTED_EDGE('',*,*,#2011,.T.);
#2853=ORIENTED_EDGE('',*,*,#2007,.F.);
#2854=ORIENTED_EDGE('',*,*,#2012,.F.);
#2855=ORIENTED_EDGE('',*,*,#1999,.T.);
#2856=ORIENTED_EDGE('',*,*,#2013,.T.);
#2857=ORIENTED_EDGE('',*,*,#2010,.F.);
#2858=ORIENTED_EDGE('',*,*,#2013,.F.);
#2859=ORIENTED_EDGE('',*,*,#1998,.F.);
#2860=ORIENTED_EDGE('',*,*,#2002,.F.);
#2861=ORIENTED_EDGE('',*,*,#2005,.F.);
#2862=ORIENTED_EDGE('',*,*,#2008,.F.);
#2863=ORIENTED_EDGE('',*,*,#2011,.F.);
#2864=ORIENTED_EDGE('',*,*,#2014,.F.);
#2865=ORIENTED_EDGE('',*,*,#2015,.T.);
#2866=ORIENTED_EDGE('',*,*,#2016,.T.);
#2867=ORIENTED_EDGE('',*,*,#2015,.F.);
#2868=ORIENTED_EDGE('',*,*,#2014,.T.);
#2869=ORIENTED_EDGE('',*,*,#1996,.T.);
#2870=ORIENTED_EDGE('',*,*,#2012,.T.);
#2871=ORIENTED_EDGE('',*,*,#2009,.T.);
#2872=ORIENTED_EDGE('',*,*,#2006,.T.);
#2873=ORIENTED_EDGE('',*,*,#2003,.T.);
#2874=ORIENTED_EDGE('',*,*,#2000,.T.);
#2875=ORIENTED_EDGE('',*,*,#2016,.F.);
#3091=CYLINDRICAL_SURFACE('',#3652,1.);
#3240=ADVANCED_FACE('',(#402),#229,.F.);
#3241=ADVANCED_FACE('',(#403),#230,.F.);
#3242=ADVANCED_FACE('',(#404),#231,.F.);
#3243=ADVANCED_FACE('',(#405),#232,.F.);
#3244=ADVANCED_FACE('',(#406),#233,.F.);
#3245=ADVANCED_FACE('',(#407),#234,.F.);
#3246=ADVANCED_FACE('',(#408),#235,.F.);
#3247=ADVANCED_FACE('',(#409),#3091,.T.);
#3248=ADVANCED_FACE('',(#410,#95),#236,.T.);
#3249=ADVANCED_FACE('',(#411),#237,.F.);
#3291=CLOSED_SHELL('',(#3240,#3241,#3242,#3243,#3244,#3245,#3246,#3247,
#3248,#3249));
#3644=AXIS2_PLACEMENT_3D('',#9510,#4408,#4409);
#3645=AXIS2_PLACEMENT_3D('',#9511,#4410,#4411);
#3646=AXIS2_PLACEMENT_3D('',#9520,#4416,#4417);
#3647=AXIS2_PLACEMENT_3D('',#9526,#4421,#4422);
#3648=AXIS2_PLACEMENT_3D('',#9532,#4426,#4427);
#3649=AXIS2_PLACEMENT_3D('',#9538,#4431,#4432);
#3650=AXIS2_PLACEMENT_3D('',#9544,#4436,#4437);
#3651=AXIS2_PLACEMENT_3D('',#9547,#4440,#4441);
#3652=AXIS2_PLACEMENT_3D('',#9548,#4442,#4443);
#3653=AXIS2_PLACEMENT_3D('',#9550,#4444,#4445);
#3654=AXIS2_PLACEMENT_3D('',#9553,#4447,#4448);
#3655=AXIS2_PLACEMENT_3D('',#9554,#4449,#4450);
#3656=AXIS2_PLACEMENT_3D('',#9555,#4451,#4452);
#4408=DIRECTION('axis',(0.,0.,1.));
#4409=DIRECTION('refdir',(1.,0.,0.));
#4410=DIRECTION('center_axis',(-0.855116261416916,0.,0.518436282932008));
#4411=DIRECTION('ref_axis',(0.518436282932008,0.,0.855116261416916));
#4412=DIRECTION('',(0.518436282932008,0.,0.855116261416916));
#4413=DIRECTION('',(0.,1.,0.));
#4414=DIRECTION('',(0.518436282932008,0.,0.855116261416916));
#4415=DIRECTION('',(0.,1.,0.));
#4416=DIRECTION('center_axis',(-0.876537121971153,0.,-0.481334264110221));
#4417=DIRECTION('ref_axis',(-0.481334264110221,0.,0.876537121971153));
#4418=DIRECTION('',(-0.481334264110221,0.,0.876537121971153));
#4419=DIRECTION('',(0.,1.,0.));
#4420=DIRECTION('',(-0.481334264110221,0.,0.876537121971153));
#4421=DIRECTION('center_axis',(-0.0214208605542369,0.,-0.999770547042228));
#4422=DIRECTION('ref_axis',(-0.999770547042228,0.,0.0214208605542369));
#4423=DIRECTION('',(-0.999770547042228,0.,0.0214208605542369));
#4424=DIRECTION('',(0.,1.,0.));
#4425=DIRECTION('',(-0.999770547042228,0.,0.0214208605542369));
#4426=DIRECTION('center_axis',(0.855116261416916,0.,-0.518436282932007));
#4427=DIRECTION('ref_axis',(-0.518436282932007,0.,-0.855116261416916));
#4428=DIRECTION('',(-0.518436282932007,0.,-0.855116261416916));
#4429=DIRECTION('',(0.,1.,0.));
#4430=DIRECTION('',(-0.518436282932007,0.,-0.855116261416916));
#4431=DIRECTION('center_axis',(0.876537121971153,0.,0.481334264110221));
#4432=DIRECTION('ref_axis',(0.481334264110221,0.,-0.876537121971153));
#4433=DIRECTION('',(0.481334264110221,0.,-0.876537121971153));
#4434=DIRECTION('',(0.,1.,0.));
#4435=DIRECTION('',(0.481334264110221,0.,-0.876537121971153));
#4436=DIRECTION('center_axis',(0.0214208605542369,0.,0.999770547042228));
#4437=DIRECTION('ref_axis',(0.999770547042228,0.,-0.0214208605542369));
#4438=DIRECTION('',(0.999770547042228,0.,-0.0214208605542369));
#4439=DIRECTION('',(0.999770547042228,0.,-0.0214208605542369));
#4440=DIRECTION('center_axis',(0.,1.,0.));
#4441=DIRECTION('ref_axis',(0.,0.,1.));
#4442=DIRECTION('center_axis',(0.,-1.,0.));
#4443=DIRECTION('ref_axis',(1.,0.,0.));
#4444=DIRECTION('center_axis',(0.,-1.,0.));
#4445=DIRECTION('ref_axis',(1.,0.,0.));
#4446=DIRECTION('',(0.,1.,0.));
#4447=DIRECTION('center_axis',(0.,-1.,0.));
#4448=DIRECTION('ref_axis',(1.,0.,0.));
#4449=DIRECTION('center_axis',(0.,-1.,0.));
#4450=DIRECTION('ref_axis',(1.,0.,0.));
#4451=DIRECTION('center_axis',(0.,-1.,0.));
#4452=DIRECTION('ref_axis',(1.,0.,0.));
#9510=CARTESIAN_POINT('',(0.,0.,0.));
#9511=CARTESIAN_POINT('Origin',(-0.57721779446269,-7.,9.01236733960726));
#9512=CARTESIAN_POINT('',(-0.57721779446269,-7.,9.01236733960726));
#9513=CARTESIAN_POINT('',(-0.277898466954226,-7.,9.50606894332475));
#9514=CARTESIAN_POINT('',(-0.502387962585574,-7.,9.13579274053664));
#9515=CARTESIAN_POINT('',(-0.57721779446269,-6.6,9.01236733960726));
#9516=CARTESIAN_POINT('',(-0.57721779446269,-7.,9.01236733960726));
#9517=CARTESIAN_POINT('',(-0.277898466954226,-6.6,9.50606894332475));
#9518=CARTESIAN_POINT('',(-0.277898466954226,-6.6,9.50606894332475));
#9519=CARTESIAN_POINT('',(-0.277898466954226,-7.,9.50606894332475));
#9520=CARTESIAN_POINT('Origin',(-0.299319327508464,-7.,8.50629839628252));
#9521=CARTESIAN_POINT('',(-0.299319327508464,-7.,8.50629839628252));
#9522=CARTESIAN_POINT('',(-0.36879394424702,-7.,8.6328156321137));
#9523=CARTESIAN_POINT('',(-0.299319327508464,-6.6,8.50629839628252));
#9524=CARTESIAN_POINT('',(-0.299319327508464,-7.,8.50629839628252));
#9525=CARTESIAN_POINT('',(-0.57721779446269,-6.6,9.01236733960726));
#9526=CARTESIAN_POINT('Origin',(0.277898466954227,-7.,8.49393105667526));
#9527=CARTESIAN_POINT('',(0.277898466954227,-7.,8.49393105667526));
#9528=CARTESIAN_POINT('',(0.133594018338554,-7.,8.49702289157707));
#9529=CARTESIAN_POINT('',(0.277898466954227,-6.6,8.49393105667526));
#9530=CARTESIAN_POINT('',(0.277898466954227,-7.,8.49393105667526));
#9531=CARTESIAN_POINT('',(-0.299319327508464,-6.6,8.50629839628252));
#9532=CARTESIAN_POINT('Origin',(0.57721779446269,-7.,8.98763266039274));
#9533=CARTESIAN_POINT('',(0.57721779446269,-7.,8.98763266039274));
#9534=CARTESIAN_POINT('',(0.502387962585574,-7.,8.86420725946337));
#9535=CARTESIAN_POINT('',(0.57721779446269,-6.6,8.98763266039274));
#9536=CARTESIAN_POINT('',(0.57721779446269,-7.,8.98763266039274));
#9537=CARTESIAN_POINT('',(0.277898466954227,-6.6,8.49393105667526));
#9538=CARTESIAN_POINT('Origin',(0.299319327508464,-7.,9.49370160371748));
#9539=CARTESIAN_POINT('',(0.299319327508464,-7.,9.49370160371748));
#9540=CARTESIAN_POINT('',(0.36879394424702,-7.,9.3671843678863));
#9541=CARTESIAN_POINT('',(0.299319327508464,-6.6,9.49370160371748));
#9542=CARTESIAN_POINT('',(0.299319327508464,-7.,9.49370160371748));
#9543=CARTESIAN_POINT('',(0.57721779446269,-6.6,8.98763266039274));
#9544=CARTESIAN_POINT('Origin',(-0.277898466954226,-7.,9.50606894332475));
#9545=CARTESIAN_POINT('',(-0.133594018338554,-7.,9.50297710842293));
#9546=CARTESIAN_POINT('',(0.299319327508464,-6.6,9.49370160371748));
#9547=CARTESIAN_POINT('Origin',(6.93889390390723E-17,-6.6,9.));
#9548=CARTESIAN_POINT('Origin',(0.,-6.,9.));
#9549=CARTESIAN_POINT('',(-1.,-7.,9.));
#9550=CARTESIAN_POINT('Origin',(0.,-7.,9.));
#9551=CARTESIAN_POINT('',(-1.,-6.,9.));
#9552=CARTESIAN_POINT('',(-1.,-6.,9.));
#9553=CARTESIAN_POINT('Origin',(0.,-6.,9.));
#9554=CARTESIAN_POINT('Origin',(0.,-7.,9.));
#9555=CARTESIAN_POINT('Origin',(0.,-6.,9.));
#9805=UNCERTAINTY_MEASURE_WITH_UNIT(LENGTH_MEASURE(0.01),#9823,
'DISTANCE_ACCURACY_VALUE',
'Maximum model space distance between geometric entities at asserted c
onnectivities');
#9811=UNCERTAINTY_MEASURE_WITH_UNIT(LENGTH_MEASURE(0.01),#9823,
'DISTANCE_ACCURACY_VALUE',
'Maximum model space distance between geometric entities at asserted c
onnectivities');
#9816=(
GEOMETRIC_REPRESENTATION_CONTEXT(3)
GLOBAL_UNCERTAINTY_ASSIGNED_CONTEXT((#9805))
GLOBAL_UNIT_ASSIGNED_CONTEXT((#9823,#9825,#9826))
REPRESENTATION_CONTEXT('','3D')
);
#9822=(
GEOMETRIC_REPRESENTATION_CONTEXT(3)
GLOBAL_UNCERTAINTY_ASSIGNED_CONTEXT((#9811))
GLOBAL_UNIT_ASSIGNED_CONTEXT((#9823,#9825,#9826))
REPRESENTATION_CONTEXT('','3D')
);
#9823=(
LENGTH_UNIT()
NAMED_UNIT(*)
SI_UNIT(.MILLI.,.METRE.)
);
#9825=(
NAMED_UNIT(*)
PLANE_ANGLE_UNIT()
SI_UNIT($,.RADIAN.)
);
#9826=(
NAMED_UNIT(*)
SI_UNIT($,.STERADIAN.)
SOLID_ANGLE_UNIT()
);
#9831=SHAPE_DEFINITION_REPRESENTATION(#9841,#9860);
#9841=PRODUCT_DEFINITION_SHAPE('',$,#9871);
#9860=SHAPE_REPRESENTATION('',(#3644),#9816);
#9866=PRODUCT_DEFINITION_CONTEXT('part definition',#9898,'design');
#9871=PRODUCT_DEFINITION('Screw_01','Screw_01',#9881,#9866);
#9881=PRODUCT_DEFINITION_FORMATION('',$,#9904);
#9898=APPLICATION_CONTEXT(
'Core Data for Automotive Mechanical Design Process');
#9899=PRODUCT_CONTEXT('part definition',#9898,'mechanical');
#9904=PRODUCT('Screw_01','Screw_01',$,(#9899));
#9912=PRESENTATION_STYLE_ASSIGNMENT((#9915));
#9915=SURFACE_STYLE_USAGE(.BOTH.,#9918);
#9918=SURFACE_SIDE_STYLE('',(#9921));
#9921=SURFACE_STYLE_FILL_AREA(#9924);
#9924=FILL_AREA_STYLE('Opaque(233,233,233)',(#9927));
#9927=FILL_AREA_STYLE_COLOUR('Opaque(233,233,233)',#9930);
#9930=COLOUR_RGB('Opaque(233,233,233)', 0.40784314, 0.44705882, 0.49803922);
ENDSEC;
END-ISO-10303-21;
